ISO-10303-21;
HEADER;
/* Generated by software containing ST-Developer
 * from STEP Tools, Inc. (www.steptools.com) 
 */

FILE_DESCRIPTION(
/* description */ ('Bin tilter linkage'),
/* implementation_level */ '2;1');

FILE_NAME(
/* name */ 'Guide bearing retainer (1).step',
/* time_stamp */ '2026-10-28T03:26:24-07:00',
/* author */ (''),
/* organization */ (''),
/* preprocessor_version */ 'ST-DEVELOPER v20.2',
/* originating_system */ 'Autodesk Translation Framework v15.17.0.0',
/* authorisation */ '');

FILE_SCHEMA (('AUTOMOTIVE_DESIGN { 1 0 10303 214 3 1 1 }'));
ENDSEC;

DATA;
#10=MECHANICAL_DESIGN_GEOMETRIC_PRESENTATION_REPRESENTATION('',(#962),#23728);
#742=SHAPE_REPRESENTATION_RELATIONSHIP('SRR','None',#24211,#848);
#848=ADVANCED_BREP_SHAPE_REPRESENTATION('',(#1074),#23711);
#962=STYLED_ITEM('',(#24765),#1074);
#1074=MANIFOLD_SOLID_BREP('Body1',#12494);
#1456=FACE_BOUND('',#3723,.T.);
#1457=FACE_BOUND('',#3724,.T.);
#1458=FACE_BOUND('',#3725,.T.);
#1459=FACE_BOUND('',#3727,.T.);
#1460=FACE_BOUND('',#3728,.T.);
#1461=FACE_BOUND('',#3729,.T.);
#1828=PLANE('',#15269);
#1829=PLANE('',#15270);
#1830=PLANE('',#15271);
#1831=PLANE('',#15272);
#1832=PLANE('',#15273);
#1833=PLANE('',#15274);
#2569=FACE_OUTER_BOUND('',#3715,.T.);
#2570=FACE_OUTER_BOUND('',#3716,.T.);
#2571=FACE_OUTER_BOUND('',#3717,.T.);
#2572=FACE_OUTER_BOUND('',#3718,.T.);
#2573=FACE_OUTER_BOUND('',#3719,.T.);
#2574=FACE_OUTER_BOUND('',#3720,.T.);
#2575=FACE_OUTER_BOUND('',#3721,.T.);
#2576=FACE_OUTER_BOUND('',#3722,.T.);
#2577=FACE_OUTER_BOUND('',#3726,.T.);
#3715=EDGE_LOOP('',(#10913,#10914,#10915,#10916));
#3716=EDGE_LOOP('',(#10917,#10918,#10919,#10920));
#3717=EDGE_LOOP('',(#10921,#10922,#10923,#10924));
#3718=EDGE_LOOP('',(#10925,#10926,#10927,#10928));
#3719=EDGE_LOOP('',(#10929,#10930,#10931,#10932));
#3720=EDGE_LOOP('',(#10933,#10934,#10935,#10936));
#3721=EDGE_LOOP('',(#10937,#10938,#10939,#10940));
#3722=EDGE_LOOP('',(#10941,#10942,#10943,#10944));
#3723=EDGE_LOOP('',(#10945));
#3724=EDGE_LOOP('',(#10946));
#3725=EDGE_LOOP('',(#10947));
#3726=EDGE_LOOP('',(#10948,#10949,#10950,#10951));
#3727=EDGE_LOOP('',(#10952));
#3728=EDGE_LOOP('',(#10953));
#3729=EDGE_LOOP('',(#10954));
#4422=LINE('',#23066,#5097);
#4423=LINE('',#23072,#5098);
#4424=LINE('',#23078,#5099);
#4425=LINE('',#23083,#5100);
#4426=LINE('',#23085,#5101);
#4427=LINE('',#23087,#5102);
#4428=LINE('',#23088,#5103);
#4429=LINE('',#23091,#5104);
#4430=LINE('',#23093,#5105);
#4431=LINE('',#23094,#5106);
#4432=LINE('',#23097,#5107);
#4433=LINE('',#23099,#5108);
#4434=LINE('',#23100,#5109);
#4435=LINE('',#23102,#5110);
#4436=LINE('',#23103,#5111);
#5097=VECTOR('',#19219,0.65);
#5098=VECTOR('',#19226,0.8);
#5099=VECTOR('',#19233,0.8);
#5100=VECTOR('',#19238,1.);
#5101=VECTOR('',#19239,1.);
#5102=VECTOR('',#19240,1.);
#5103=VECTOR('',#19241,1.);
#5104=VECTOR('',#19244,1.);
#5105=VECTOR('',#19245,1.);
#5106=VECTOR('',#19246,1.);
#5107=VECTOR('',#19249,1.);
#5108=VECTOR('',#19250,1.);
#5109=VECTOR('',#19251,1.);
#5110=VECTOR('',#19254,1.);
#5111=VECTOR('',#19255,1.);
#5882=CIRCLE('',#15261,0.65);
#5883=CIRCLE('',#15262,0.65);
#5884=CIRCLE('',#15264,0.8);
#5885=CIRCLE('',#15265,0.8);
#5886=CIRCLE('',#15267,0.8);
#5887=CIRCLE('',#15268,0.8);
#6809=VERTEX_POINT('',#23063);
#6810=VERTEX_POINT('',#23065);
#6811=VERTEX_POINT('',#23069);
#6812=VERTEX_POINT('',#23071);
#6813=VERTEX_POINT('',#23075);
#6814=VERTEX_POINT('',#23077);
#6815=VERTEX_POINT('',#23081);
#6816=VERTEX_POINT('',#23082);
#6817=VERTEX_POINT('',#23084);
#6818=VERTEX_POINT('',#23086);
#6819=VERTEX_POINT('',#23090);
#6820=VERTEX_POINT('',#23092);
#6821=VERTEX_POINT('',#23096);
#6822=VERTEX_POINT('',#23098);
#8196=EDGE_CURVE('',#6809,#6809,#5882,.T.);
#8197=EDGE_CURVE('',#6809,#6810,#4422,.T.);
#8198=EDGE_CURVE('',#6810,#6810,#5883,.T.);
#8199=EDGE_CURVE('',#6811,#6811,#5884,.T.);
#8200=EDGE_CURVE('',#6811,#6812,#4423,.T.);
#8201=EDGE_CURVE('',#6812,#6812,#5885,.T.);
#8202=EDGE_CURVE('',#6813,#6813,#5886,.T.);
#8203=EDGE_CURVE('',#6813,#6814,#4424,.T.);
#8204=EDGE_CURVE('',#6814,#6814,#5887,.T.);
#8205=EDGE_CURVE('',#6815,#6816,#4425,.T.);
#8206=EDGE_CURVE('',#6816,#6817,#4426,.T.);
#8207=EDGE_CURVE('',#6818,#6817,#4427,.T.);
#8208=EDGE_CURVE('',#6815,#6818,#4428,.T.);
#8209=EDGE_CURVE('',#6819,#6815,#4429,.T.);
#8210=EDGE_CURVE('',#6820,#6818,#4430,.T.);
#8211=EDGE_CURVE('',#6819,#6820,#4431,.T.);
#8212=EDGE_CURVE('',#6821,#6819,#4432,.T.);
#8213=EDGE_CURVE('',#6822,#6820,#4433,.T.);
#8214=EDGE_CURVE('',#6821,#6822,#4434,.T.);
#8215=EDGE_CURVE('',#6816,#6821,#4435,.T.);
#8216=EDGE_CURVE('',#6817,#6822,#4436,.T.);
#10913=ORIENTED_EDGE('',*,*,#8196,.F.);
#10914=ORIENTED_EDGE('',*,*,#8197,.T.);
#10915=ORIENTED_EDGE('',*,*,#8198,.F.);
#10916=ORIENTED_EDGE('',*,*,#8197,.F.);
#10917=ORIENTED_EDGE('',*,*,#8199,.F.);
#10918=ORIENTED_EDGE('',*,*,#8200,.T.);
#10919=ORIENTED_EDGE('',*,*,#8201,.F.);
#10920=ORIENTED_EDGE('',*,*,#8200,.F.);
#10921=ORIENTED_EDGE('',*,*,#8202,.F.);
#10922=ORIENTED_EDGE('',*,*,#8203,.T.);
#10923=ORIENTED_EDGE('',*,*,#8204,.F.);
#10924=ORIENTED_EDGE('',*,*,#8203,.F.);
#10925=ORIENTED_EDGE('',*,*,#8205,.T.);
#10926=ORIENTED_EDGE('',*,*,#8206,.T.);
#10927=ORIENTED_EDGE('',*,*,#8207,.F.);
#10928=ORIENTED_EDGE('',*,*,#8208,.F.);
#10929=ORIENTED_EDGE('',*,*,#8209,.T.);
#10930=ORIENTED_EDGE('',*,*,#8208,.T.);
#10931=ORIENTED_EDGE('',*,*,#8210,.F.);
#10932=ORIENTED_EDGE('',*,*,#8211,.F.);
#10933=ORIENTED_EDGE('',*,*,#8212,.T.);
#10934=ORIENTED_EDGE('',*,*,#8211,.T.);
#10935=ORIENTED_EDGE('',*,*,#8213,.F.);
#10936=ORIENTED_EDGE('',*,*,#8214,.F.);
#10937=ORIENTED_EDGE('',*,*,#8215,.T.);
#10938=ORIENTED_EDGE('',*,*,#8214,.T.);
#10939=ORIENTED_EDGE('',*,*,#8216,.F.);
#10940=ORIENTED_EDGE('',*,*,#8206,.F.);
#10941=ORIENTED_EDGE('',*,*,#8216,.T.);
#10942=ORIENTED_EDGE('',*,*,#8213,.T.);
#10943=ORIENTED_EDGE('',*,*,#8210,.T.);
#10944=ORIENTED_EDGE('',*,*,#8207,.T.);
#10945=ORIENTED_EDGE('',*,*,#8198,.T.);
#10946=ORIENTED_EDGE('',*,*,#8201,.T.);
#10947=ORIENTED_EDGE('',*,*,#8204,.T.);
#10948=ORIENTED_EDGE('',*,*,#8215,.F.);
#10949=ORIENTED_EDGE('',*,*,#8205,.F.);
#10950=ORIENTED_EDGE('',*,*,#8209,.F.);
#10951=ORIENTED_EDGE('',*,*,#8212,.F.);
#10952=ORIENTED_EDGE('',*,*,#8196,.T.);
#10953=ORIENTED_EDGE('',*,*,#8199,.T.);
#10954=ORIENTED_EDGE('',*,*,#8202,.T.);
#11582=CYLINDRICAL_SURFACE('',#15260,0.65);
#11583=CYLINDRICAL_SURFACE('',#15263,0.8);
#11584=CYLINDRICAL_SURFACE('',#15266,0.8);
#12294=ADVANCED_FACE('',(#2569),#11582,.F.);
#12295=ADVANCED_FACE('',(#2570),#11583,.F.);
#12296=ADVANCED_FACE('',(#2571),#11584,.F.);
#12297=ADVANCED_FACE('',(#2572),#1828,.T.);
#12298=ADVANCED_FACE('',(#2573),#1829,.T.);
#12299=ADVANCED_FACE('',(#2574),#1830,.T.);
#12300=ADVANCED_FACE('',(#2575),#1831,.T.);
#12301=ADVANCED_FACE('',(#2576,#1456,#1457,#1458),#1832,.T.);
#12302=ADVANCED_FACE('',(#2577,#1459,#1460,#1461),#1833,.F.);
#12494=CLOSED_SHELL('',(#12294,#12295,#12296,#12297,#12298,#12299,#12300,
#12301,#12302));
#15259=AXIS2_PLACEMENT_3D('',#23061,#19213,#19214);
#15260=AXIS2_PLACEMENT_3D('',#23062,#19215,#19216);
#15261=AXIS2_PLACEMENT_3D('',#23064,#19217,#19218);
#15262=AXIS2_PLACEMENT_3D('',#23067,#19220,#19221);
#15263=AXIS2_PLACEMENT_3D('',#23068,#19222,#19223);
#15264=AXIS2_PLACEMENT_3D('',#23070,#19224,#19225);
#15265=AXIS2_PLACEMENT_3D('',#23073,#19227,#19228);
#15266=AXIS2_PLACEMENT_3D('',#23074,#19229,#19230);
#15267=AXIS2_PLACEMENT_3D('',#23076,#19231,#19232);
#15268=AXIS2_PLACEMENT_3D('',#23079,#19234,#19235);
#15269=AXIS2_PLACEMENT_3D('',#23080,#19236,#19237);
#15270=AXIS2_PLACEMENT_3D('',#23089,#19242,#19243);
#15271=AXIS2_PLACEMENT_3D('',#23095,#19247,#19248);
#15272=AXIS2_PLACEMENT_3D('',#23101,#19252,#19253);
#15273=AXIS2_PLACEMENT_3D('',#23104,#19256,#19257);
#15274=AXIS2_PLACEMENT_3D('',#23105,#19258,#19259);
#19213=DIRECTION('axis',(0.,0.,1.));
#19214=DIRECTION('refdir',(1.,0.,0.));
#19215=DIRECTION('center_axis',(1.,0.,0.));
#19216=DIRECTION('ref_axis',(0.,0.,-1.));
#19217=DIRECTION('center_axis',(1.,0.,0.));
#19218=DIRECTION('ref_axis',(0.,0.,-1.));
#19219=DIRECTION('',(1.,0.,0.));
#19220=DIRECTION('center_axis',(-1.,0.,0.));
#19221=DIRECTION('ref_axis',(0.,0.,-1.));
#19222=DIRECTION('center_axis',(1.,0.,0.));
#19223=DIRECTION('ref_axis',(0.,0.,-1.));
#19224=DIRECTION('center_axis',(1.,0.,0.));
#19225=DIRECTION('ref_axis',(0.,0.,-1.));
#19226=DIRECTION('',(1.,0.,0.));
#19227=DIRECTION('center_axis',(-1.,0.,0.));
#19228=DIRECTION('ref_axis',(0.,0.,-1.));
#19229=DIRECTION('center_axis',(1.,0.,0.));
#19230=DIRECTION('ref_axis',(0.,0.,-1.));
#19231=DIRECTION('center_axis',(1.,0.,0.));
#19232=DIRECTION('ref_axis',(0.,0.,-1.));
#19233=DIRECTION('',(1.,0.,0.));
#19234=DIRECTION('center_axis',(-1.,0.,0.));
#19235=DIRECTION('ref_axis',(0.,0.,-1.));
#19236=DIRECTION('center_axis',(0.,0.,1.));
#19237=DIRECTION('ref_axis',(0.,-1.,0.));
#19238=DIRECTION('',(0.,-1.,0.));
#19239=DIRECTION('',(1.,0.,0.));
#19240=DIRECTION('',(0.,-1.,0.));
#19241=DIRECTION('',(1.,0.,0.));
#19242=DIRECTION('center_axis',(0.,1.,0.));
#19243=DIRECTION('ref_axis',(0.,0.,1.));
#19244=DIRECTION('',(0.,0.,1.));
#19245=DIRECTION('',(0.,0.,1.));
#19246=DIRECTION('',(1.,0.,0.));
#19247=DIRECTION('center_axis',(0.,0.,-1.));
#19248=DIRECTION('ref_axis',(0.,1.,0.));
#19249=DIRECTION('',(0.,1.,0.));
#19250=DIRECTION('',(0.,1.,0.));
#19251=DIRECTION('',(1.,0.,0.));
#19252=DIRECTION('center_axis',(0.,-1.,0.));
#19253=DIRECTION('ref_axis',(0.,0.,-1.));
#19254=DIRECTION('',(0.,0.,-1.));
#19255=DIRECTION('',(0.,0.,-1.));
#19256=DIRECTION('center_axis',(1.,0.,0.));
#19257=DIRECTION('ref_axis',(0.,0.,-1.));
#19258=DIRECTION('center_axis',(1.,0.,0.));
#19259=DIRECTION('ref_axis',(0.,0.,-1.));
#23061=CARTESIAN_POINT('',(0.,0.,0.));
#23062=CARTESIAN_POINT('Origin',(-2.4,-4.5,8.));
#23063=CARTESIAN_POINT('',(-2.3,-4.5,8.65));
#23064=CARTESIAN_POINT('Origin',(-2.3,-4.5,8.));
#23065=CARTESIAN_POINT('',(-2.1,-4.5,8.65));
#23066=CARTESIAN_POINT('',(-2.4,-4.5,8.65));
#23067=CARTESIAN_POINT('Origin',(-2.1,-4.5,8.));
#23068=CARTESIAN_POINT('Origin',(-2.4,-7.,8.));
#23069=CARTESIAN_POINT('',(-2.3,-7.,8.8));
#23070=CARTESIAN_POINT('Origin',(-2.3,-7.,8.));
#23071=CARTESIAN_POINT('',(-2.1,-7.,8.8));
#23072=CARTESIAN_POINT('',(-2.4,-7.,8.8));
#23073=CARTESIAN_POINT('Origin',(-2.1,-7.,8.));
#23074=CARTESIAN_POINT('Origin',(-2.4,-2.,8.));
#23075=CARTESIAN_POINT('',(-2.3,-2.,8.8));
#23076=CARTESIAN_POINT('Origin',(-2.3,-2.,8.));
#23077=CARTESIAN_POINT('',(-2.1,-2.,8.8));
#23078=CARTESIAN_POINT('',(-2.4,-2.,8.8));
#23079=CARTESIAN_POINT('Origin',(-2.1,-2.,8.));
#23080=CARTESIAN_POINT('Origin',(-2.3,-0.8,9.7));
#23081=CARTESIAN_POINT('',(-2.3,-0.8,9.7));
#23082=CARTESIAN_POINT('',(-2.3,-8.2,9.7));
#23083=CARTESIAN_POINT('',(-2.3,-0.8,9.7));
#23084=CARTESIAN_POINT('',(-2.1,-8.2,9.7));
#23085=CARTESIAN_POINT('',(-2.3,-8.2,9.7));
#23086=CARTESIAN_POINT('',(-2.1,-0.8,9.7));
#23087=CARTESIAN_POINT('',(-2.1,-0.8,9.7));
#23088=CARTESIAN_POINT('',(-2.3,-0.8,9.7));
#23089=CARTESIAN_POINT('Origin',(-2.3,-0.8,6.3));
#23090=CARTESIAN_POINT('',(-2.3,-0.8,6.3));
#23091=CARTESIAN_POINT('',(-2.3,-0.8,6.3));
#23092=CARTESIAN_POINT('',(-2.1,-0.8,6.3));
#23093=CARTESIAN_POINT('',(-2.1,-0.8,6.3));
#23094=CARTESIAN_POINT('',(-2.3,-0.8,6.3));
#23095=CARTESIAN_POINT('Origin',(-2.3,-8.2,6.3));
#23096=CARTESIAN_POINT('',(-2.3,-8.2,6.3));
#23097=CARTESIAN_POINT('',(-2.3,-8.2,6.3));
#23098=CARTESIAN_POINT('',(-2.1,-8.2,6.3));
#23099=CARTESIAN_POINT('',(-2.1,-8.2,6.3));
#23100=CARTESIAN_POINT('',(-2.3,-8.2,6.3));
#23101=CARTESIAN_POINT('Origin',(-2.3,-8.2,9.7));
#23102=CARTESIAN_POINT('',(-2.3,-8.2,9.7));
#23103=CARTESIAN_POINT('',(-2.1,-8.2,9.7));
#23104=CARTESIAN_POINT('Origin',(-2.1,-4.5,8.));
#23105=CARTESIAN_POINT('Origin',(-2.3,-4.5,8.));
#23594=UNCERTAINTY_MEASURE_WITH_UNIT(LENGTH_MEASURE(0.001),#23729,
'DISTANCE_ACCURACY_VALUE',
'Maximum model space distance between geometric entities at asserted c
onnectivities');
#23611=UNCERTAINTY_MEASURE_WITH_UNIT(LENGTH_MEASURE(0.001),#23729,
'DISTANCE_ACCURACY_VALUE',
'Maximum model space distance between geometric entities at asserted c
onnectivities');
#23711=(
GEOMETRIC_REPRESENTATION_CONTEXT(3)
GLOBAL_UNCERTAINTY_ASSIGNED_CONTEXT((#23594))
GLOBAL_UNIT_ASSIGNED_CONTEXT((#23729,#23731,#23732))
REPRESENTATION_CONTEXT('','3D')
);
#23728=(
GEOMETRIC_REPRESENTATION_CONTEXT(3)
GLOBAL_UNCERTAINTY_ASSIGNED_CONTEXT((#23611))
GLOBAL_UNIT_ASSIGNED_CONTEXT((#23729,#23731,#23732))
REPRESENTATION_CONTEXT('','3D')
);
#23729=(
LENGTH_UNIT()
NAMED_UNIT(*)
SI_UNIT(.CENTI.,.METRE.)
);
#23731=(
NAMED_UNIT(*)
PLANE_ANGLE_UNIT()
SI_UNIT($,.RADIAN.)
);
#23732=(
NAMED_UNIT(*)
SI_UNIT($,.STERADIAN.)
SOLID_ANGLE_UNIT()
);
#23832=SHAPE_DEFINITION_REPRESENTATION(#24070,#24211);
#24070=PRODUCT_DEFINITION_SHAPE('',$,#24328);
#24211=SHAPE_REPRESENTATION('',(#15259),#23711);
#24228=PRODUCT_DEFINITION_CONTEXT('part definition',#24578,'design');
#24328=PRODUCT_DEFINITION('Guide bearing retainer (1)',
'Guide bearing retainer (1)',#24444,#24228);
#24444=PRODUCT_DEFINITION_FORMATION('',$,#24679);
#24578=APPLICATION_CONTEXT(
'Core Data for Automotive Mechanical Design Process');
#24579=PRODUCT_CONTEXT('part definition',#24578,'mechanical');
#24679=PRODUCT('Guide bearing retainer (1)','Guide bearing retainer (1)',
'Guide bearing retainer (1)',(#24579));
#24759=COLOUR_RGB('Grey',0.48,0.52,0.57);
#24760=FILL_AREA_STYLE_COLOUR('',#24759);
#24761=FILL_AREA_STYLE('',(#24760));
#24762=SURFACE_STYLE_FILL_AREA(#24761);
#24763=SURFACE_SIDE_STYLE('',(#24762));
#24764=SURFACE_STYLE_USAGE(.BOTH.,#24763);
#24765=PRESENTATION_STYLE_ASSIGNMENT((#24764));
ENDSEC;
END-ISO-10303-21;
